ISO-10303-21;
HEADER;
/* Generated by software containing ST-Developer
 * from STEP Tools, Inc. (www.steptools.com) 
 */

FILE_DESCRIPTION(
/* description */ ('Independent direct-acting normally-closed roller-plunger limit-switch
 CAD. Removable cover, insulated terminal supports, captured bus/conta
ct bridge, native Coil return spring, integral lower travel stop, reus
able instanced hardware and free roller. Manual geometric contact open
ing4mm; no snap-action/contact-force, electrical/current/voltage, envi
ronmental seal, safety-switch, wear, load or life certification. Exter
nal wiring and anchors omitted; fits and application engineering requi
red.'),
/* implementation_level */ '2;1');

FILE_NAME(
/* name */ 'Roller thrust washer.step',
/* time_stamp */ '2026-11-08T07:32:43-08:00',
/* author */ (''),
/* organization */ (''),
/* preprocessor_version */ 'ST-DEVELOPER v20.2',
/* originating_system */ 'Autodesk Translation Framework v15.17.0.0',
/* authorisation */ '');

FILE_SCHEMA (('AUTOMOTIVE_DESIGN { 1 0 10303 214 3 1 1 }'));
ENDSEC;

DATA;
#10=MECHANICAL_DESIGN_GEOMETRIC_PRESENTATION_REPRESENTATION('',(#189),#36482);
#155=SHAPE_REPRESENTATION_RELATIONSHIP('SRR','None',#36568,#172);
#172=ADVANCED_BREP_SHAPE_REPRESENTATION('',(#206),#36478);
#189=STYLED_ITEM('',(#36661),#206);
#206=MANIFOLD_SOLID_BREP('Body1',#9780);
#294=FACE_BOUND('',#1437,.T.);
#295=FACE_BOUND('',#1439,.T.);
#407=PLANE('',#10503);
#408=PLANE('',#10504);
#837=FACE_OUTER_BOUND('',#1434,.T.);
#838=FACE_OUTER_BOUND('',#1435,.T.);
#839=FACE_OUTER_BOUND('',#1436,.T.);
#840=FACE_OUTER_BOUND('',#1438,.T.);
#1434=EDGE_LOOP('',(#8104,#8105,#8106,#8107));
#1435=EDGE_LOOP('',(#8108,#8109,#8110,#8111));
#1436=EDGE_LOOP('',(#8112));
#1437=EDGE_LOOP('',(#8113));
#1438=EDGE_LOOP('',(#8114));
#1439=EDGE_LOOP('',(#8115));
#1713=CIRCLE('',#10498,0.2);
#1714=CIRCLE('',#10499,0.2);
#1715=CIRCLE('',#10501,0.4);
#1716=CIRCLE('',#10502,0.4);
#2869=LINE('',#29645,#3443);
#2870=LINE('',#29651,#3444);
#3443=VECTOR('',#12168,0.2);
#3444=VECTOR('',#12175,0.4);
#4297=VERTEX_POINT('',#29642);
#4298=VERTEX_POINT('',#29644);
#4299=VERTEX_POINT('',#29648);
#4300=VERTEX_POINT('',#29650);
#5608=EDGE_CURVE('',#4297,#4297,#1713,.T.);
#5609=EDGE_CURVE('',#4297,#4298,#2869,.T.);
#5610=EDGE_CURVE('',#4298,#4298,#1714,.T.);
#5611=EDGE_CURVE('',#4299,#4299,#1715,.T.);
#5612=EDGE_CURVE('',#4299,#4300,#2870,.T.);
#5613=EDGE_CURVE('',#4300,#4300,#1716,.T.);
#8104=ORIENTED_EDGE('',*,*,#5608,.F.);
#8105=ORIENTED_EDGE('',*,*,#5609,.T.);
#8106=ORIENTED_EDGE('',*,*,#5610,.T.);
#8107=ORIENTED_EDGE('',*,*,#5609,.F.);
#8108=ORIENTED_EDGE('',*,*,#5611,.F.);
#8109=ORIENTED_EDGE('',*,*,#5612,.T.);
#8110=ORIENTED_EDGE('',*,*,#5613,.T.);
#8111=ORIENTED_EDGE('',*,*,#5612,.F.);
#8112=ORIENTED_EDGE('',*,*,#5611,.T.);
#8113=ORIENTED_EDGE('',*,*,#5608,.T.);
#8114=ORIENTED_EDGE('',*,*,#5613,.F.);
#8115=ORIENTED_EDGE('',*,*,#5610,.F.);
#9130=CYLINDRICAL_SURFACE('',#10497,0.2);
#9131=CYLINDRICAL_SURFACE('',#10500,0.4);
#9627=ADVANCED_FACE('',(#837),#9130,.F.);
#9628=ADVANCED_FACE('',(#838),#9131,.T.);
#9629=ADVANCED_FACE('',(#839,#294),#407,.T.);
#9630=ADVANCED_FACE('',(#840,#295),#408,.F.);
#9780=CLOSED_SHELL('',(#9627,#9628,#9629,#9630));
#10496=AXIS2_PLACEMENT_3D('',#29640,#12162,#12163);
#10497=AXIS2_PLACEMENT_3D('',#29641,#12164,#12165);
#10498=AXIS2_PLACEMENT_3D('',#29643,#12166,#12167);
#10499=AXIS2_PLACEMENT_3D('',#29646,#12169,#12170);
#10500=AXIS2_PLACEMENT_3D('',#29647,#12171,#12172);
#10501=AXIS2_PLACEMENT_3D('',#29649,#12173,#12174);
#10502=AXIS2_PLACEMENT_3D('',#29652,#12176,#12177);
#10503=AXIS2_PLACEMENT_3D('',#29653,#12178,#12179);
#10504=AXIS2_PLACEMENT_3D('',#29654,#12180,#12181);
#12162=DIRECTION('axis',(0.,0.,1.));
#12163=DIRECTION('refdir',(1.,0.,0.));
#12164=DIRECTION('center_axis',(0.,0.,1.));
#12165=DIRECTION('ref_axis',(1.,0.,0.));
#12166=DIRECTION('center_axis',(0.,0.,-1.));
#12167=DIRECTION('ref_axis',(1.,0.,0.));
#12168=DIRECTION('',(0.,0.,-1.));
#12169=DIRECTION('center_axis',(0.,0.,-1.));
#12170=DIRECTION('ref_axis',(1.,0.,0.));
#12171=DIRECTION('center_axis',(0.,0.,1.));
#12172=DIRECTION('ref_axis',(1.,0.,0.));
#12173=DIRECTION('center_axis',(0.,0.,1.));
#12174=DIRECTION('ref_axis',(1.,0.,0.));
#12175=DIRECTION('',(0.,0.,-1.));
#12176=DIRECTION('center_axis',(0.,0.,1.));
#12177=DIRECTION('ref_axis',(1.,0.,0.));
#12178=DIRECTION('center_axis',(0.,0.,1.));
#12179=DIRECTION('ref_axis',(1.,0.,0.));
#12180=DIRECTION('center_axis',(0.,0.,1.));
#12181=DIRECTION('ref_axis',(1.,0.,0.));
#29640=CARTESIAN_POINT('',(0.,0.,0.));
#29641=CARTESIAN_POINT('Origin',(0.,0.,0.));
#29642=CARTESIAN_POINT('',(-0.2,-2.44929359829471E-17,0.1));
#29643=CARTESIAN_POINT('Origin',(0.,0.,0.1));
#29644=CARTESIAN_POINT('',(-0.2,-2.44929359829471E-17,0.));
#29645=CARTESIAN_POINT('',(-0.2,-2.44929359829471E-17,0.));
#29646=CARTESIAN_POINT('Origin',(0.,0.,0.));
#29647=CARTESIAN_POINT('Origin',(0.,0.,0.));
#29648=CARTESIAN_POINT('',(-0.4,-4.89858719658941E-17,0.1));
#29649=CARTESIAN_POINT('Origin',(0.,0.,0.1));
#29650=CARTESIAN_POINT('',(-0.4,-4.89858719658941E-17,0.));
#29651=CARTESIAN_POINT('',(-0.4,-4.89858719658941E-17,0.));
#29652=CARTESIAN_POINT('Origin',(0.,0.,0.));
#29653=CARTESIAN_POINT('Origin',(0.,0.,0.1));
#29654=CARTESIAN_POINT('Origin',(0.,0.,0.));
#36459=UNCERTAINTY_MEASURE_WITH_UNIT(LENGTH_MEASURE(0.001),#36483,
'DISTANCE_ACCURACY_VALUE',
'Maximum model space distance between geometric entities at asserted c
onnectivities');
#36463=UNCERTAINTY_MEASURE_WITH_UNIT(LENGTH_MEASURE(0.001),#36483,
'DISTANCE_ACCURACY_VALUE',
'Maximum model space distance between geometric entities at asserted c
onnectivities');
#36478=(
GEOMETRIC_REPRESENTATION_CONTEXT(3)
GLOBAL_UNCERTAINTY_ASSIGNED_CONTEXT((#36459))
GLOBAL_UNIT_ASSIGNED_CONTEXT((#36483,#36485,#36486))
REPRESENTATION_CONTEXT('','3D')
);
#36482=(
GEOMETRIC_REPRESENTATION_CONTEXT(3)
GLOBAL_UNCERTAINTY_ASSIGNED_CONTEXT((#36463))
GLOBAL_UNIT_ASSIGNED_CONTEXT((#36483,#36485,#36486))
REPRESENTATION_CONTEXT('','3D')
);
#36483=(
LENGTH_UNIT()
NAMED_UNIT(*)
SI_UNIT(.CENTI.,.METRE.)
);
#36485=(
NAMED_UNIT(*)
PLANE_ANGLE_UNIT()
SI_UNIT($,.RADIAN.)
);
#36486=(
NAMED_UNIT(*)
SI_UNIT($,.STERADIAN.)
SOLID_ANGLE_UNIT()
);
#36501=SHAPE_DEFINITION_REPRESENTATION(#36519,#36568);
#36519=PRODUCT_DEFINITION_SHAPE('',$,#36587);
#36568=SHAPE_REPRESENTATION('',(#10496),#36478);
#36572=PRODUCT_DEFINITION_CONTEXT('part definition',#36628,'design');
#36587=PRODUCT_DEFINITION('Roller thrust washer','Roller thrust washer',
#36605,#36572);
#36605=PRODUCT_DEFINITION_FORMATION('',$,#36644);
#36628=APPLICATION_CONTEXT(
'Core Data for Automotive Mechanical Design Process');
#36629=PRODUCT_CONTEXT('part definition',#36628,'mechanical');
#36644=PRODUCT('Roller thrust washer','Roller thrust washer',$,(#36629));
#36661=PRESENTATION_STYLE_ASSIGNMENT((#36675));
#36675=SURFACE_STYLE_USAGE(.BOTH.,#36689);
#36689=SURFACE_SIDE_STYLE('',(#36703));
#36703=SURFACE_STYLE_FILL_AREA(#36717);
#36717=FILL_AREA_STYLE('Washer gray',(#36731));
#36731=FILL_AREA_STYLE_COLOUR('Washer gray',#36745);
#36745=COLOUR_RGB('Washer gray',0.725490196078431,0.752941176470588,0.792156862745098);
ENDSEC;
END-ISO-10303-21;
